ISO-10303-21;
HEADER;
FILE_DESCRIPTION (('STEP AP214'),
    '1' );
FILE_NAME ('socket head cap screw_iso_ISO 4762 M4 x 10 - 10N.step',
    '2026-10-25T07:12:54',
    ( '' ),
    ( '' ),
    'SwSTEP 2.0',
    'SolidWorks 2026',
    '' );
FILE_SCHEMA (( 'AUTOMOTIVE_DESIGN' ));
ENDSEC;

DATA;
#36=FACE_OUTER_BOUND ( 'NONE', #13516, .T. ) ;
#57=CARTESIAN_POINT ( 'NONE',  ( 2.000000000000000000, 0.000000000000000000, 0.000000000000000000 ) ) ;
#71=FACE_OUTER_BOUND ( 'NONE', #6413, .T. ) ;
#96=ORIENTED_EDGE ( 'NONE', *, *, #7070, .F. ) ;
#106=SURFACE_STYLE_USAGE ( .BOTH. , #7508 ) ;
#117=AXIS2_PLACEMENT_3D ( 'NONE', #12874, #6605, #168 ) ;
#136=AXIS2_PLACEMENT_3D ( 'NONE', #12197, #10046, #9019 ) ;
#149=ORIENTED_EDGE ( 'NONE', *, *, #1777, .T. ) ;
#160=CARTESIAN_POINT ( 'NONE',  ( 4.000000000000003553, 4.286263797015736595E-16, -3.500000000000000000 ) ) ;
#168=DIRECTION ( 'NONE',  ( 0.000000000000000000, 0.000000000000000000, 1.000000000000000000 ) ) ;
#174=FACE_OUTER_BOUND ( 'NONE', #12287, .T. ) ;
#189=CIRCLE ( 'NONE', #9683, 1.610000000000000098 ) ;
#221=CYLINDRICAL_SURFACE ( 'NONE', #6994, 2.000000000000000888 ) ;
#233=PLANE ( 'NONE',  #5515 ) ;
#242=DIRECTION ( 'NONE',  ( 1.000000000000000000, 0.000000000000000000, 0.000000000000000000 ) ) ;
#305=DIRECTION ( 'NONE',  ( 0.000000000000000000, 0.000000000000000000, -1.000000000000000000 ) ) ;
#316=DIRECTION ( 'NONE',  ( -0.000000000000000000, 1.000000000000000000, 1.224646799147353207E-16 ) ) ;
#324=DIRECTION ( 'NONE',  ( 0.000000000000000000, 0.000000000000000000, 1.000000000000000000 ) ) ;
#340=CARTESIAN_POINT ( 'NONE',  ( 2.000000000000000000, 1.773042676681340524, -2.059984127722458425E-15 ) ) ;
#365=CARTESIAN_POINT ( 'NONE',  ( 2.000000000000000000, 0.000000000000000000, 0.000000000000000000 ) ) ;
#430=AXIS2_PLACEMENT_3D ( 'NONE', #5828, #10990, #3471 ) ;
#443=PRODUCT ( 'socket head cap screw_iso_ISO 4762 M4 x 10 - 10N', 'socket head cap screw_iso_ISO 4762 M4 x 10 - 10N', '', ( #4109 ) ) ;
#460=CARTESIAN_POINT ( 'NONE',  ( -31.74999999999995737, 0.000000000000000000, 3.500000000000000000 ) ) ;
#471=AXIS2_PLACEMENT_3D ( 'NONE', #11512, #1111, #6405 ) ;
#482=VECTOR ( 'NONE', #7003, 1000.000000000000000 ) ;
#491=CARTESIAN_POINT ( 'NONE',  ( 2.000000000000000000, -1.773042676681341856, 2.276824562219559311E-15 ) ) ;
#517=VECTOR ( 'NONE', #2587, 1000.000000000000000 ) ;
#521=EDGE_LOOP ( 'NONE', ( #1458, #5060, #12101, #1592, #7858 ) ) ;
#540=LINE ( 'NONE', #8995, #9886 ) ;
#562=PLANE ( 'NONE',  #11679 ) ;
#568=VERTEX_POINT ( 'NONE', #5098 ) ;
#572=CARTESIAN_POINT ( 'NONE',  ( 2.000000000000000000, -1.773042676681341856, 2.276824562219559311E-15 ) ) ;
#639=LINE ( 'NONE', #572, #12415 ) ;
#654=ADVANCED_FACE ( 'NONE', ( #3348 ), #233, .F. ) ;
#679=AXIS2_PLACEMENT_3D ( 'NONE', #3829, #8050, #11290 ) ;
#701=DIRECTION ( 'NONE',  ( -1.000000000000000000, -0.000000000000000000, -0.000000000000000000 ) ) ;
#777=EDGE_CURVE ( 'NONE', #10184, #6619, #3754, .T. ) ;
#793=ORIENTED_EDGE ( 'NONE', *, *, #2126, .T. ) ;
#795=MECHANICAL_DESIGN_GEOMETRIC_PRESENTATION_REPRESENTATION('',(#3898),#6353);
#835=DIRECTION ( 'NONE',  ( 0.000000000000000000, -0.5000000000000011102, -0.8660254037844379305 ) ) ;
#889=DIRECTION ( 'NONE',  ( -0.7071067811865350272, 8.659560562355083235E-17, -0.7071067811865598962 ) ) ;
#922=ORIENTED_EDGE ( 'NONE', *, *, #10131, .F. ) ;
#958=CIRCLE ( 'NONE', #7613, 0.2000000000000000944 ) ;
#970=VECTOR ( 'NONE', #4699, 1000.000000000000000 ) ;
#973=DIRECTION ( 'NONE',  ( 0.000000000000000000, 0.000000000000000000, -1.000000000000000000 ) ) ;
#987=ORIENTED_EDGE ( 'NONE', *, *, #1362, .T. ) ;
#1042=CARTESIAN_POINT ( 'NONE',  ( 2.000000000000000000, 1.773042676681340524, -2.059984127722458425E-15 ) ) ;
#1050=VERTEX_POINT ( 'NONE', #12862 ) ;
#1057=FILL_AREA_STYLE ('',( #7645 ) ) ;
#1093=ADVANCED_FACE ( 'NONE', ( #2423 ), #221, .T. ) ;
#1111=DIRECTION ( 'NONE',  ( 0.000000000000000000, 0.8660254037844380415, -0.5000000000000012212 ) ) ;
#1133=CIRCLE ( 'NONE', #4918, 1.535500000000000087 ) ;
#1181=LINE ( 'NONE', #1042, #8228 ) ;
#1185=CONICAL_SURFACE ( 'NONE', #3190, 1.610000000000000098, 0.7853981633974658205 ) ;
#1187=MANIFOLD_SOLID_BREP ( 'Hex', #8467 ) ;
#1201=FACE_OUTER_BOUND ( 'NONE', #4084, .T. ) ;
#1215=CARTESIAN_POINT ( 'NONE',  ( 2.000000000000000000, 0.8865213383406680414, -1.535500000000000975 ) ) ;
#1225=CIRCLE ( 'NONE', #10946, 3.500000000000000000 ) ;
#1237=DIRECTION ( 'NONE',  ( 0.000000000000000000, -1.000000000000000000, 0.000000000000000000 ) ) ;
#1255=CARTESIAN_POINT ( 'NONE',  ( 2.000000000000000000, 1.773042676681340524, -2.059984127722458425E-15 ) ) ;
#1307=FACE_OUTER_BOUND ( 'NONE', #8603, .T. ) ;
#1313=PLANE ( 'NONE',  #8899 ) ;
#1331=CARTESIAN_POINT ( 'NONE',  ( 4.200000000000001954, 0.000000000000000000, 0.000000000000000000 ) ) ;
#1344=EDGE_CURVE ( 'NONE', #9289, #5152, #12504, .T. ) ;
#1348=EDGE_CURVE ( 'NONE', #11125, #10197, #10580, .T. ) ;
#1362=EDGE_CURVE ( 'NONE', #11343, #10542, #12586, .T. ) ;
#1392=DIRECTION ( 'NONE',  ( 0.000000000000000000, 0.000000000000000000, -1.000000000000000000 ) ) ;
#1396=DIRECTION ( 'NONE',  ( 0.000000000000000000, 0.000000000000000000, -1.000000000000000000 ) ) ;
#1404=EDGE_CURVE ( 'NONE', #10542, #9688, #11623, .T. ) ;
#1438=ADVANCED_FACE ( 'NONE', ( #71 ), #7660, .F. ) ;
#1445=CARTESIAN_POINT ( 'NONE',  ( -31.74999999999995737, 0.000000000000000000, 0.000000000000000000 ) ) ;
#1457=DIRECTION ( 'NONE',  ( 1.000000000000000000, 0.000000000000000000, 0.000000000000000000 ) ) ;
#1458=ORIENTED_EDGE ( 'NONE', *, *, #5839, .F. ) ;
#1500=EDGE_CURVE ( 'NONE', #2486, #10197, #9207, .T. ) ;
#1525=ORIENTED_EDGE ( 'NONE', *, *, #12483, .F. ) ;
#1541=ORIENTED_EDGE ( 'NONE', *, *, #8366, .F. ) ;
#1592=ORIENTED_EDGE ( 'NONE', *, *, #4472, .T. ) ;
#1609=EDGE_LOOP ( 'NONE', ( #9856, #13113, #12373, #3824, #12071, #9555 ) ) ;
#1613=EDGE_CURVE ( 'NONE', #10197, #2486, #13552, .T. ) ;
#1630=ORIENTED_EDGE ( 'NONE', *, *, #5441, .F. ) ;
#1662=ORIENTED_EDGE ( 'NONE', *, *, #5497, .T. ) ;
#1674=FACE_OUTER_BOUND ( 'NONE', #521, .T. ) ;
#1682=ORIENTED_EDGE ( 'NONE', *, *, #3729, .F. ) ;
#1688=DIRECTION ( 'NONE',  ( 0.000000000000000000, 0.000000000000000000, 1.000000000000000000 ) ) ;
#1715=ORIENTED_EDGE ( 'NONE', *, *, #3585, .F. ) ;
#1723=DIRECTION ( 'NONE',  ( 0.000000000000000000, 0.8660254037844380415, -0.5000000000000012212 ) ) ;
#1736=CARTESIAN_POINT ( 'NONE',  ( 2.000000000000000000, 1.773042676681340524, -2.059984127722458425E-15 ) ) ;
#1739=DIRECTION ( 'NONE',  ( -1.000000000000000000, -0.000000000000000000, -0.000000000000000000 ) ) ;
#1756=CARTESIAN_POINT ( 'NONE',  ( 13.99999999999999822, 0.000000000000000000, 0.000000000000000000 ) ) ;
#1765=CARTESIAN_POINT ( 'NONE',  ( 2.000000000000000000, -1.773042676681341856, 2.276824562219559311E-15 ) ) ;
#1777=EDGE_CURVE ( 'NONE', #6619, #9080, #12238, .T. ) ;
#1798=EDGE_CURVE ( 'NONE', #10006, #10542, #11868, .T. ) ;
#1826=EDGE_LOOP ( 'NONE', ( #11523, #11071, #5516, #8412 ) ) ;
#1858=CIRCLE ( 'NONE', #5194, 2.200000000000001066 ) ;
#1946=EDGE_CURVE ( 'NONE', #2436, #11305, #3639, .T. ) ;
#1986=DIRECTION ( 'NONE',  ( 0.000000000000000000, 0.000000000000000000, 1.000000000000000000 ) ) ;
#2021=DIRECTION ( 'NONE',  ( 0.000000000000000000, -0.4999999999999991118, 0.8660254037844391517 ) ) ;
#2026=CARTESIAN_POINT ( 'NONE',  ( 2.000000000000000000, 1.329782007511004727, -0.7677500000000018199 ) ) ;
#2063=CARTESIAN_POINT ( 'NONE',  ( 2.000000000000000000, 0.8865213383406680414, -1.535500000000000975 ) ) ;
#2126=EDGE_CURVE ( 'NONE', #1050, #2821, #12187, .T. ) ;
#2137=DIRECTION ( 'NONE',  ( 0.000000000000000000, -1.000000000000000000, 9.783878858594328898E-16 ) ) ;
#2158=CARTESIAN_POINT ( 'NONE',  ( 0.1999999999999987899, 0.000000000000000000, 3.500000000000000000 ) ) ;
#2163=VERTEX_POINT ( 'NONE', #5576 ) ;
#2170=TOROIDAL_SURFACE ( 'NONE', #5722, 2.200000000000001066, 0.2000000000000000111 ) ;
#2182=AXIS2_PLACEMENT_3D ( 'NONE', #12816, #8688, #1396 ) ;
#2192=DIRECTION ( 'NONE',  ( -1.000000000000000000, 0.000000000000000000, -0.000000000000000000 ) ) ;
#2199=EDGE_LOOP ( 'NONE', ( #1525, #5702, #7813, #5010 ) ) ;
#2203=TOROIDAL_SURFACE ( 'NONE', #11708, 2.200000000000001066, 0.2000000000000000111 ) ;
#2211=ORIENTED_EDGE ( 'NONE', *, *, #1613, .T. ) ;
#2240=DIRECTION ( 'NONE',  ( 0.000000000000000000, 0.000000000000000000, -1.000000000000000000 ) ) ;
#2247=ORIENTED_EDGE ( 'NONE', *, *, #7828, .F. ) ;
#2285=DIRECTION ( 'NONE',  ( 0.000000000000000000, 0.000000000000000000, 1.000000000000000000 ) ) ;
#2294=CARTESIAN_POINT ( 'NONE',  ( -31.74999999999995737, 0.000000000000000000, 0.000000000000000000 ) ) ;
#2303=ORIENTED_EDGE ( 'NONE', *, *, #7828, .T. ) ;
#2332=ORIENTED_EDGE ( 'NONE', *, *, #6924, .F. ) ;
#2333=ORIENTED_EDGE ( 'NONE', *, *, #6132, .F. ) ;
#2337=VECTOR ( 'NONE', #889, 1000.000000000000114 ) ;
#2377=PLANE ( 'NONE',  #11010 ) ;
#2385=DIRECTION ( 'NONE',  ( 1.000000000000000000, 0.000000000000000000, 0.000000000000000000 ) ) ;
#2403=AXIS2_PLACEMENT_3D ( 'NONE', #9410, #3184, #12582 ) ;
#2422=DIRECTION ( 'NONE',  ( -1.000000000000000000, -0.000000000000000000, -0.000000000000000000 ) ) ;
#2423=FACE_OUTER_BOUND ( 'NONE', #4572, .T. ) ;
#2429=CARTESIAN_POINT ( 'NONE',  ( 2.000000000000000000, 1.773042676681340524, -2.059984127722458425E-15 ) ) ;
#2436=VERTEX_POINT ( 'NONE', #3900 ) ;
#2449=ORIENTED_EDGE ( 'NONE', *, *, #4923, .T. ) ;
#2451=ADVANCED_FACE ( 'NONE', ( #1674 ), #10115, .T. ) ;
#2465=EDGE_CURVE ( 'NONE', #13025, #2854, #1225, .T. ) ;
#2486=VERTEX_POINT ( 'NONE', #13086 ) ;
#2496=DIRECTION ( 'NONE',  ( -1.000000000000000000, -0.000000000000000000, -0.000000000000000000 ) ) ;
#2505=VECTOR ( 'NONE', #8545, 1000.000000000000000 ) ;
#2506=ORIENTED_EDGE ( 'NONE', *, *, #3585, .T. ) ;
#2518=CARTESIAN_POINT ( 'NONE',  ( -31.74999999999995737, 2.449293598294707893E-16, -2.000000000000000888 ) ) ;
#2519=ORIENTED_EDGE ( 'NONE', *, *, #777, .F. ) ;
#2531=CARTESIAN_POINT ( 'NONE',  ( 2.000000000000000000, 0.000000000000000000, 0.000000000000000000 ) ) ;
#2561=EDGE_CURVE ( 'NONE', #9809, #2590, #12608, .T. ) ;
#2587=DIRECTION ( 'NONE',  ( -1.000000000000000000, -0.000000000000000000, -0.000000000000000000 ) ) ;
#2590=VERTEX_POINT ( 'NONE', #4247 ) ;
#2630=( NAMED_UNIT ( * ) PLANE_ANGLE_UNIT ( ) SI_UNIT ( $, .RADIAN. ) );
#2647=ORIENTED_EDGE ( 'NONE', *, *, #1404, .T. ) ;
#2776=DIRECTION ( 'NONE',  ( 0.000000000000000000, 0.5000000000000011102, 0.8660254037844379305 ) ) ;
#2782=CARTESIAN_POINT ( 'NONE',  ( 2.000000000000000000, 0.000000000000000000, 1.535500000000000087 ) ) ;
#2803=ADVANCED_FACE ( 'NONE', ( #8672 ), #10867, .T. ) ;
#2821=VERTEX_POINT ( 'NONE', #9702 ) ;
#2854=VERTEX_POINT ( 'NONE', #160 ) ;
#2909=FACE_BOUND ( 'NONE', #6769, .T. ) ;
#2937=CARTESIAN_POINT ( 'NONE',  ( 0.000000000000000000, -0.8865213383406694847, 1.535500000000001419 ) ) ;
#2952=CARTESIAN_POINT ( 'NONE',  ( 0.000000000000000000, -1.773042676681341856, 2.276824562219559311E-15 ) ) ;
#2964=ADVANCED_FACE ( 'NONE', ( #10795 ), #1313, .F. ) ;
#2977=EDGE_CURVE ( 'NONE', #7203, #11927, #7905, .T. ) ;
#2978=ORIENTED_EDGE ( 'NONE', *, *, #7070, .T. ) ;
#3015=DIRECTION ( 'NONE',  ( -1.000000000000000000, -0.000000000000000000, -0.000000000000000000 ) ) ;
#3016=VECTOR ( 'NONE', #835, 1000.000000000000114 ) ;
#3037=CARTESIAN_POINT ( 'NONE',  ( 13.99999999999999822, 0.000000000000000000, 0.000000000000000000 ) ) ;
#3078=( GEOMETRIC_REPRESENTATION_CONTEXT ( 3 ) GLOBAL_UNCERTAINTY_ASSIGNED_CONTEXT ( ( #3700 ) ) GLOBAL_UNIT_ASSIGNED_CONTEXT ( ( #6003, #10342, #9445 ) ) REPRESENTATION_CONTEXT ( 'NONE', 'WORKASPACE' ) );
#3088=LINE ( 'NONE', #2952, #7700 ) ;
#3105=FACE_BOUND ( 'NONE', #1609, .T. ) ;
#3112=ORIENTED_EDGE ( 'NONE', *, *, #2465, .F. ) ;
#3113=EDGE_LOOP ( 'NONE', ( #7723, #4903, #5534, #149, #4501 ) ) ;
#3123=CIRCLE ( 'NONE', #5124, 0.2000000000000000944 ) ;
#3130=EDGE_CURVE ( 'NONE', #7203, #11305, #10998, .T. ) ;
#3132=CARTESIAN_POINT ( 'NONE',  ( 0.000000000000000000, 0.000000000000000000, 0.000000000000000000 ) ) ;
#3135=CIRCLE ( 'NONE', #7992, 1.610000000000000098 ) ;
#3172=DIRECTION ( 'NONE',  ( 0.000000000000000000, -1.000000000000000000, 0.000000000000000000 ) ) ;
#3175=DIRECTION ( 'NONE',  ( 0.000000000000000000, 1.000000000000000000, -9.783878858594328898E-16 ) ) ;
#3184=DIRECTION ( 'NONE',  ( 1.000000000000000000, 0.000000000000000000, 0.000000000000000000 ) ) ;
#3190=AXIS2_PLACEMENT_3D ( 'NONE', #11990, #10040, #12057 ) ;
#3201=LINE ( 'NONE', #8456, #10986 ) ;
#3210=FACE_OUTER_BOUND ( 'NONE', #7045, .T. ) ;
#3247=AXIS2_PLACEMENT_3D ( 'NONE', #4020, #7350, #8515 ) ;
#3264=ORIENTED_EDGE ( 'NONE', *, *, #1348, .T. ) ;
#3329=VERTEX_POINT ( 'NONE', #6452 ) ;
#3348=FACE_OUTER_BOUND ( 'NONE', #8041, .T. ) ;
#3349=ORIENTED_EDGE ( 'NONE', *, *, #6379, .T. ) ;
#3363=LINE ( 'NONE', #2518, #10704 ) ;
#3369=CARTESIAN_POINT ( 'NONE',  ( 4.200000000000001954, 0.000000000000000000, 0.000000000000000000 ) ) ;
#3375=VECTOR ( 'NONE', #5698, 1000.000000000000000 ) ;
#3385=VERTEX_POINT ( 'NONE', #9480 ) ;
#3450=ORIENTED_EDGE ( 'NONE', *, *, #4766, .F. ) ;
#3465=ORIENTED_EDGE ( 'NONE', *, *, #11081, .T. ) ;
#3466=EDGE_LOOP ( 'NONE', ( #12772, #3532, #11763 ) ) ;
#3471=DIRECTION ( 'NONE',  ( 1.000000000000000000, 0.000000000000000000, 0.000000000000000000 ) ) ;
#3523=DIRECTION ( 'NONE',  ( -1.000000000000000000, -0.000000000000000000, -0.000000000000000000 ) ) ;
#3532=ORIENTED_EDGE ( 'NONE', *, *, #4472, .F. ) ;
#3585=EDGE_CURVE ( 'NONE', #6619, #9887, #8785, .T. ) ;
#3587=ORIENTED_EDGE ( 'NONE', *, *, #5113, .F. ) ;
#3590=ORIENTED_EDGE ( 'NONE', *, *, #1777, .F. ) ;
#3631=CIRCLE ( 'NONE', #11360, 1.535500000000000087 ) ;
#3639=CIRCLE ( 'NONE', #12681, 1.535500000000000087 ) ;
#3649=LINE ( 'NONE', #1765, #4522 ) ;
#3698=PLANE ( 'NONE',  #9602 ) ;
#3700=UNCERTAINTY_MEASURE_WITH_UNIT (LENGTH_MEASURE( 1.000000000000000082E-05 ), #6003, 'distance_accuracy_value', 'NONE');
#3729=EDGE_CURVE ( 'NONE', #9887, #3329, #9592, .T. ) ;
#3744=CIRCLE ( 'NONE', #13249, 0.2000000000000000944 ) ;
#3754=LINE ( 'NONE', #1736, #7736 ) ;
#3777=DIRECTION ( 'NONE',  ( 0.000000000000000000, 0.000000000000000000, 1.000000000000000000 ) ) ;
#3805=ORIENTED_EDGE ( 'NONE', *, *, #8150, .F. ) ;
#3809=DIRECTION ( 'NONE',  ( 1.000000000000000000, 0.000000000000000000, 0.000000000000000000 ) ) ;
#3824=ORIENTED_EDGE ( 'NONE', *, *, #5839, .T. ) ;
#3829=CARTESIAN_POINT ( 'NONE',  ( 4.000000000000003553, 0.000000000000000000, 0.000000000000000000 ) ) ;
#3887=EDGE_LOOP ( 'NONE', ( #8727, #8328, #6236, #96 ) ) ;
#3898=STYLED_ITEM('',(#13712),#1187);
#3900=CARTESIAN_POINT ( 'NONE',  ( 2.000000000000000000, -1.329782007511005837, 0.7677500000000023750 ) ) ;
#3908=EDGE_CURVE ( 'NONE', #10197, #5875, #3363, .T. ) ;
#3965=CARTESIAN_POINT ( 'NONE',  ( 13.99999999999999822, 0.000000000000000000, 1.610000000000000098 ) ) ;
#3971=CIRCLE ( 'NONE', #10155, 1.535500000000000087 ) ;
#3981=AXIS2_PLACEMENT_3D ( 'NONE', #1255, #5448, #2240 ) ;
#4020=CARTESIAN_POINT ( 'NONE',  ( 0.1999999999999987899, 0.000000000000000000, 0.000000000000000000 ) ) ;
#4025=CONICAL_SURFACE ( 'NONE', #11746, 1.535500000000000087, 1.047197551196590748 ) ;
#4032=UNCERTAINTY_MEASURE_WITH_UNIT (LENGTH_MEASURE( 1.000000000000000082E-05 ), #7764, 'distance_accuracy_value', 'NONE');
#4033=EDGE_LOOP ( 'NONE', ( #12118, #10245, #5979, #10985 ) ) ;
#4061=CARTESIAN_POINT ( 'NONE',  ( 2.000000000000000000, 1.773042676681340524, -2.059984127722458425E-15 ) ) ;
#4077=PLANE ( 'NONE',  #8844 ) ;
#4084=EDGE_LOOP ( 'NONE', ( #8343, #1715, #8828 ) ) ;
#4090=EDGE_CURVE ( 'NONE', #7440, #9688, #10196, .T. ) ;
#4094=CARTESIAN_POINT ( 'NONE',  ( 13.99999999999999822, 1.971681346627238735E-16, -1.610000000000000098 ) ) ;
#4109=PRODUCT_CONTEXT ( 'NONE', #4778, 'mechanical' ) ;
#4127=ADVANCED_FACE ( 'NONE', ( #4955 ), #3698, .F. ) ;
#4150=ORIENTED_EDGE ( 'NONE', *, *, #12102, .T. ) ;
#4164=CIRCLE ( 'NONE', #8582, 2.000000000000000888 ) ;
#4166=ORIENTED_EDGE ( 'NONE', *, *, #4226, .T. ) ;
#4170=CARTESIAN_POINT ( 'NONE',  ( 2.000000000000000000, 1.773042676681340524, -2.059984127722458425E-15 ) ) ;
#4204=ORIENTED_EDGE ( 'NONE', *, *, #7972, .T. ) ;
#4226=EDGE_CURVE ( 'NONE', #9486, #3385, #1858, .T. ) ;
#4242=AXIS2_PLACEMENT_3D ( 'NONE', #12250, #9406, #10033 ) ;
#4247=CARTESIAN_POINT ( 'NONE',  ( 0.000000000000000000, -1.773042676681341856, 2.276824562219559311E-15 ) ) ;
#4253=ORIENTED_EDGE ( 'NONE', *, *, #4923, .F. ) ;
#4254=VECTOR ( 'NONE', #9105, 1000.000000000000000 ) ;
#4314=CARTESIAN_POINT ( 'NONE',  ( 2.000000000000000000, 1.773042676681340524, -2.059984127722458425E-15 ) ) ;
#4322=CARTESIAN_POINT ( 'NONE',  ( 0.000000000000000000, 1.773042676681340524, -2.059984127722458425E-15 ) ) ;
#4354=ORIENTED_EDGE ( 'NONE', *, *, #12989, .F. ) ;
#4421=EDGE_LOOP ( 'NONE', ( #2519, #13394, #3590 ) ) ;
#4440=CARTESIAN_POINT ( 'NONE',  ( -31.74999999999995737, 0.000000000000000000, 0.000000000000000000 ) ) ;
#4457=SURFACE_STYLE_FILL_AREA ( #1057 ) ;
#4462=LINE ( 'NONE', #10813, #10363 ) ;
#4472=EDGE_CURVE ( 'NONE', #2163, #7440, #3649, .T. ) ;
#4501=ORIENTED_EDGE ( 'NONE', *, *, #8150, .T. ) ;
#4522=VECTOR ( 'NONE', #7105, 1000.000000000000227 ) ;
#4566=DIRECTION ( 'NONE',  ( 0.000000000000000000, -0.4999999999999991118, 0.8660254037844391517 ) ) ;
#4572=EDGE_LOOP ( 'NONE', ( #6523, #2211, #10972, #11094 ) ) ;
#4576=EDGE_CURVE ( 'NONE', #8730, #2436, #11033, .T. ) ;
#4588=ORIENTED_EDGE ( 'NONE', *, *, #3729, .T. ) ;
#4608=CIRCLE ( 'NONE', #12767, 3.500000000000000000 ) ;
#4615=LINE ( 'NONE', #13163, #13068 ) ;
#4632=CARTESIAN_POINT ( 'NONE',  ( 2.000000000000000000, 1.773042676681340524, -2.059984127722458425E-15 ) ) ;
#4699=DIRECTION ( 'NONE',  ( -1.000000000000000000, -0.000000000000000000, -0.000000000000000000 ) ) ;
#4710=VECTOR ( 'NONE', #4566, 1000.000000000000000 ) ;
#4765=DIRECTION ( 'NONE',  ( 1.000000000000000000, 0.000000000000000000, 0.000000000000000000 ) ) ;
#4766=EDGE_CURVE ( 'NONE', #10184, #9080, #9318, .T. ) ;
#4778=APPLICATION_CONTEXT ( 'automotive_design' ) ;
#4798=DIRECTION ( 'NONE',  ( 0.000000000000000000, 0.4999999999999989453, -0.8660254037844391517 ) ) ;
#4806=CARTESIAN_POINT ( 'NONE',  ( 2.000000000000000000, -0.8865213383406694847, 1.535500000000001419 ) ) ;
#4818=CARTESIAN_POINT ( 'NONE',  ( 0.000000000000000000, 0.000000000000000000, 0.000000000000000000 ) ) ;
#4843=MECHANICAL_DESIGN_GEOMETRIC_PRESENTATION_REPRESENTATION('',(#8604),#10132);
#4880=DIRECTION ( 'NONE',  ( 0.000000000000000000, 0.000000000000000000, 1.000000000000000000 ) ) ;
#4903=ORIENTED_EDGE ( 'NONE', *, *, #3130, .T. ) ;
#4918=AXIS2_PLACEMENT_3D ( 'NONE', #12543, #12670, #8268 ) ;
#4923=EDGE_CURVE ( 'NONE', #7907, #2486, #11154, .T. ) ;
#4955=FACE_OUTER_BOUND ( 'NONE', #11712, .T. ) ;
#5007=ORIENTED_EDGE ( 'NONE', *, *, #13177, .F. ) ;
#5010=ORIENTED_EDGE ( 'NONE', *, *, #2126, .F. ) ;
#5034=ADVANCED_FACE ( 'NONE', ( #3210 ), #9432, .F. ) ;
#5060=ORIENTED_EDGE ( 'NONE', *, *, #6966, .F. ) ;
#5096=DIRECTION ( 'NONE',  ( 0.000000000000000000, 0.000000000000000000, -1.000000000000000000 ) ) ;
#5098=CARTESIAN_POINT ( 'NONE',  ( 4.200000000000001954, 0.000000000000000000, 2.000000000000000888 ) ) ;
#5103=CARTESIAN_POINT ( 'NONE',  ( 2.000000000000000000, -0.8865213383406730374, -1.535499999999999421 ) ) ;
#5113=EDGE_CURVE ( 'NONE', #9080, #10006, #1181, .T. ) ;
#5124=AXIS2_PLACEMENT_3D ( 'NONE', #12829, #3172, #8560 ) ;
#5131=CIRCLE ( 'NONE', #679, 3.500000000000000000 ) ;
#5152=VERTEX_POINT ( 'NONE', #2158 ) ;
#5180=DIRECTION ( 'NONE',  ( 0.000000000000000000, -0.5000000000000011102, -0.8660254037844379305 ) ) ;
#5194=AXIS2_PLACEMENT_3D ( 'NONE', #10470, #10333, #5096 ) ;
#5199=AXIS2_PLACEMENT_3D ( 'NONE', #6113, #7209, #8316 ) ;
#5208=PLANE ( 'NONE',  #2403 ) ;
#5209=CIRCLE ( 'NONE', #12905, 0.2000000000000000944 ) ;
#5215=ADVANCED_FACE ( 'NONE', ( #10733 ), #7634, .T. ) ;
#5229=DIRECTION ( 'NONE',  ( 0.000000000000000000, 1.000000000000000000, -1.224646799147353207E-16 ) ) ;
#5340=CARTESIAN_POINT ( 'NONE',  ( 0.000000000000000000, 1.773042676681340524, -2.059984127722458425E-15 ) ) ;
#5346=CIRCLE ( 'NONE', #7991, 3.299999999999999822 ) ;
#5441=EDGE_CURVE ( 'NONE', #5875, #568, #10639, .T. ) ;
#5448=DIRECTION ( 'NONE',  ( 1.000000000000000000, 0.000000000000000000, 0.000000000000000000 ) ) ;
#5460=CARTESIAN_POINT ( 'NONE',  ( 0.1999999999999987899, 4.041334437186265510E-16, -3.299999999999999822 ) ) ;
#5471=ORIENTED_EDGE ( 'NONE', *, *, #1348, .F. ) ;
#5497=EDGE_CURVE ( 'NONE', #11125, #7907, #3135, .T. ) ;
#5501=CARTESIAN_POINT ( 'NONE',  ( 2.000000000000000000, 2.065682573263594481E-15, 1.535500000000000309 ) ) ;
#5515=AXIS2_PLACEMENT_3D ( 'NONE', #12806, #1457, #7503 ) ;
#5516=ORIENTED_EDGE ( 'NONE', *, *, #7972, .F. ) ;
#5534=ORIENTED_EDGE ( 'NONE', *, *, #9649, .T. ) ;
#5548=AXIS2_PLACEMENT_3D ( 'NONE', #12981, #8923, #10978 ) ;
#5553=DIRECTION ( 'NONE',  ( 0.000000000000000000, 0.000000000000000000, 1.000000000000000000 ) ) ;
#5576=CARTESIAN_POINT ( 'NONE',  ( 2.000000000000000000, -1.329782007511007169, -0.7677499999999988223 ) ) ;
#5613=ORIENTED_EDGE ( 'NONE', *, *, #4576, .F. ) ;
#5622=DIRECTION ( 'NONE',  ( -1.000000000000000000, -0.000000000000000000, -0.000000000000000000 ) ) ;
#5677=PLANE ( 'NONE',  #5548 ) ;
#5691=DIRECTION ( 'NONE',  ( 0.000000000000000000, 0.000000000000000000, 1.000000000000000000 ) ) ;
#5698=DIRECTION ( 'NONE',  ( -0.5000000000000061062, 1.060575238724902601E-16, -0.8660254037844351549 ) ) ;
#5702=ORIENTED_EDGE ( 'NONE', *, *, #10572, .F. ) ;
#5705=ORIENTED_EDGE ( 'NONE', *, *, #12012, .F. ) ;
#5720=ORIENTED_EDGE ( 'NONE', *, *, #3130, .F. ) ;
#5722=AXIS2_PLACEMENT_3D ( 'NONE', #1331, #6490, #12884 ) ;
#5777=ADVANCED_FACE ( 'NONE', ( #11657 ), #2170, .F. ) ;
#5784=FACE_OUTER_BOUND ( 'NONE', #2199, .T. ) ;
#5800=CARTESIAN_POINT ( 'NONE',  ( 2.000000000000000000, 0.8865213383406715941, 1.535499999999999199 ) ) ;
#5805=EDGE_CURVE ( 'NONE', #8730, #9809, #12556, .T. ) ;
#5828=CARTESIAN_POINT ( 'NONE',  ( 0.000000000000000000, 0.000000000000000000, 0.000000000000000000 ) ) ;
#5839=EDGE_CURVE ( 'NONE', #2590, #9688, #3088, .T. ) ;
#5875=VERTEX_POINT ( 'NONE', #11385 ) ;
#5923=ORIENTED_EDGE ( 'NONE', *, *, #9081, .F. ) ;
#5979=ORIENTED_EDGE ( 'NONE', *, *, #1344, .T. ) ;
#5989=VECTOR ( 'NONE', #3523, 1000.000000000000000 ) ;
#6003=( LENGTH_UNIT ( ) NAMED_UNIT ( * ) SI_UNIT ( .MILLI., .METRE. ) );
#6024=AXIS2_PLACEMENT_3D ( 'NONE', #4818, #13232, #3777 ) ;
#6038=ADVANCED_FACE ( 'NONE', ( #174 ), #2377, .T. ) ;
#6043=CARTESIAN_POINT ( 'NONE',  ( 2.000000000000000000, -0.8865213383406694847, 1.535500000000001419 ) ) ;
#6074=ORIENTED_EDGE ( 'NONE', *, *, #1946, .T. ) ;
#6113=CARTESIAN_POINT ( 'NONE',  ( 13.61000000000001009, 0.000000000000000000, 0.000000000000000000 ) ) ;
#6132=EDGE_CURVE ( 'NONE', #3385, #9486, #7496, .T. ) ;
#6133=EDGE_CURVE ( 'NONE', #11305, #9887, #4462, .T. ) ;
#6162=DIRECTION ( 'NONE',  ( -1.000000000000000000, -0.000000000000000000, -0.000000000000000000 ) ) ;
#6176=VECTOR ( 'NONE', #6290, 1000.000000000000000 ) ;
#6181=DIRECTION ( 'NONE',  ( 0.000000000000000000, 0.000000000000000000, 1.000000000000000000 ) ) ;
#6202=DIRECTION ( 'NONE',  ( 0.000000000000000000, -0.5000000000000011102, -0.8660254037844379305 ) ) ;
#6236=ORIENTED_EDGE ( 'NONE', *, *, #4226, .F. ) ;
#6269=CARTESIAN_POINT ( 'NONE',  ( 0.1999999999999987899, 0.000000000000000000, 3.299999999999999822 ) ) ;
#6272=CARTESIAN_POINT ( 'NONE',  ( 4.200000000000001954, 2.694222958124178486E-16, 2.200000000000001066 ) ) ;
#6273=ADVANCED_FACE ( 'NONE', ( #10047 ), #562, .F. ) ;
#6290=DIRECTION ( 'NONE',  ( -1.000000000000000000, -0.000000000000000000, -0.000000000000000000 ) ) ;
#6293=ADVANCED_FACE ( 'NONE', ( #5784 ), #13434, .T. ) ;
#6321=DIRECTION ( 'NONE',  ( 0.000000000000000000, -0.5000000000000011102, -0.8660254037844379305 ) ) ;
#6353=( GEOMETRIC_REPRESENTATION_CONTEXT ( 3 ) GLOBAL_UNCERTAINTY_ASSIGNED_CONTEXT ( ( #4032 ) ) GLOBAL_UNIT_ASSIGNED_CONTEXT ( ( #7764, #2630, #12177 ) ) REPRESENTATION_CONTEXT ( 'NONE', 'WORKASPACE' ) );
#6354=( LENGTH_UNIT ( ) NAMED_UNIT ( * ) SI_UNIT ( .MILLI., .METRE. ) );
#6364=DIRECTION ( 'NONE',  ( 0.000000000000000000, 0.000000000000000000, -1.000000000000000000 ) ) ;
#6370=FACE_OUTER_BOUND ( 'NONE', #10300, .T. ) ;
#6379=EDGE_CURVE ( 'NONE', #11927, #2163, #1133, .T. ) ;
#6390=ORIENTED_EDGE ( 'NONE', *, *, #8708, .T. ) ;
#6405=DIRECTION ( 'NONE',  ( 0.000000000000000000, 0.5000000000000011102, 0.8660254037844379305 ) ) ;
#6406=DIRECTION ( 'NONE',  ( 0.000000000000000000, -0.8660254037844391517, -0.4999999999999991673 ) ) ;
#6413=EDGE_LOOP ( 'NONE', ( #5720, #12993, #3349, #8543, #6074 ) ) ;
#6433=DIRECTION ( 'NONE',  ( -1.000000000000000000, -0.000000000000000000, -0.000000000000000000 ) ) ;
#6436=DIRECTION ( 'NONE',  ( -0.000000000000000000, 0.000000000000000000, 1.000000000000000000 ) ) ;
#6441=ORIENTED_EDGE ( 'NONE', *, *, #6132, .T. ) ;
#6452=CARTESIAN_POINT ( 'NONE',  ( 0.000000000000000000, 0.8865213383406715941, 1.535499999999999199 ) ) ;
#6490=DIRECTION ( 'NONE',  ( 1.000000000000000000, 0.000000000000000000, 0.000000000000000000 ) ) ;
#6523=ORIENTED_EDGE ( 'NONE', *, *, #3908, .F. ) ;
#6525=ORIENTED_EDGE ( 'NONE', *, *, #10359, .T. ) ;
#6605=DIRECTION ( 'NONE',  ( -1.000000000000000000, -0.000000000000000000, -0.000000000000000000 ) ) ;
#6619=VERTEX_POINT ( 'NONE', #8104 ) ;
#6644=CARTESIAN_POINT ( 'NONE',  ( 2.000000000000000000, -0.8865213383406694847, 1.535500000000001419 ) ) ;
#6680=CARTESIAN_POINT ( 'NONE',  ( 4.200000000000001954, 0.000000000000000000, 0.000000000000000000 ) ) ;
#6690=AXIS2_PLACEMENT_3D ( 'NONE', #4314, #6406, #9838 ) ;
#6706=ORIENTED_EDGE ( 'NONE', *, *, #4090, .F. ) ;
#6751=DIRECTION ( 'NONE',  ( -1.000000000000000000, -0.000000000000000000, -0.000000000000000000 ) ) ;
#6769=EDGE_LOOP ( 'NONE', ( #4166, #6441 ) ) ;
#6775=VECTOR ( 'NONE', #6321, 1000.000000000000114 ) ;
#6777=CARTESIAN_POINT ( 'NONE',  ( 0.1999999999999987899, 4.286263797015736595E-16, -3.500000000000000000 ) ) ;
#6784=ADVANCED_FACE ( 'NONE', ( #7414 ), #4025, .F. ) ;
#6792=DIRECTION ( 'NONE',  ( 0.000000000000000000, 0.000000000000000000, 1.000000000000000000 ) ) ;
#6801=DIRECTION ( 'NONE',  ( 0.000000000000000000, -0.4999999999999991118, 0.8660254037844391517 ) ) ;
#6822=CARTESIAN_POINT ( 'NONE',  ( 2.000000000000000000, 0.8865213383406680414, -1.535500000000000975 ) ) ;
#6862=EDGE_CURVE ( 'NONE', #11927, #7440, #9926, .T. ) ;
#6887=ORIENTED_EDGE ( 'NONE', *, *, #11081, .F. ) ;
#6906=CARTESIAN_POINT ( 'NONE',  ( 0.1999999999999987899, 0.000000000000000000, 0.000000000000000000 ) ) ;
#6924=EDGE_CURVE ( 'NONE', #10006, #11927, #4615, .T. ) ;
#6950=DIRECTION ( 'NONE',  ( -1.000000000000000000, -0.000000000000000000, -0.000000000000000000 ) ) ;
#6966=EDGE_CURVE ( 'NONE', #7271, #2590, #639, .T. ) ;
#6992=PLANE ( 'NONE',  #9259 ) ;
#6994=AXIS2_PLACEMENT_3D ( 'NONE', #4440, #2496, #5553 ) ;
#7003=DIRECTION ( 'NONE',  ( -0.5000000000000061062, 0.000000000000000000, 0.8660254037844351549 ) ) ;
#7023=CARTESIAN_POINT ( 'NONE',  ( 13.99999999999999822, 2.210487472460973684E-16, -1.610000000000000098 ) ) ;
#7042=ORIENTED_EDGE ( 'NONE', *, *, #13109, .F. ) ;
#7045=EDGE_LOOP ( 'NONE', ( #987, #12807, #3587, #3450, #6390 ) ) ;
#7060=CARTESIAN_POINT ( 'NONE',  ( 2.000000000000000000, 1.773042676681340524, -2.059984127722458425E-15 ) ) ;
#7065=PRODUCT_DEFINITION_FORMATION_WITH_SPECIFIED_SOURCE ( 'ANY', '', #443, .NOT_KNOWN. ) ;
#7070=EDGE_CURVE ( 'NONE', #5875, #9486, #3123, .T. ) ;
#7095=EDGE_LOOP ( 'NONE', ( #4354, #2303, #4150, #11317 ) ) ;
#7105=DIRECTION ( 'NONE',  ( 0.000000000000000000, 0.4999999999999989453, -0.8660254037844391517 ) ) ;
#7154=FACE_OUTER_BOUND ( 'NONE', #1826, .T. ) ;
#7175=CARTESIAN_POINT ( 'NONE',  ( 2.000000000000000000, -0.8865213383406694847, 1.535500000000001419 ) ) ;
#7194=CARTESIAN_POINT ( 'NONE',  ( 13.61000000000001009, 0.000000000000000000, 0.000000000000000000 ) ) ;
#7203=VERTEX_POINT ( 'NONE', #8904 ) ;
#7209=DIRECTION ( 'NONE',  ( -1.000000000000000000, -0.000000000000000000, -0.000000000000000000 ) ) ;
#7264=SHAPE_REPRESENTATION ( 'socket head cap screw_iso_ISO 4762 M4 x 10 - 10N', ( #430 ), #3078 ) ;
#7266=DIRECTION ( 'NONE',  ( 0.000000000000000000, 0.000000000000000000, 1.000000000000000000 ) ) ;
#7271=VERTEX_POINT ( 'NONE', #11866 ) ;
#7350=DIRECTION ( 'NONE',  ( 1.000000000000000000, 0.000000000000000000, 0.000000000000000000 ) ) ;
#7410=VECTOR ( 'NONE', #5180, 1000.000000000000114 ) ;
#7414=FACE_OUTER_BOUND ( 'NONE', #3113, .T. ) ;
#7423=ORIENTED_EDGE ( 'NONE', *, *, #8708, .F. ) ;
#7440=VERTEX_POINT ( 'NONE', #5103 ) ;
#7446=AXIS2_PLACEMENT_3D ( 'NONE', #7476, #8444, #6181 ) ;
#7472=ORIENTED_EDGE ( 'NONE', *, *, #3908, .T. ) ;
#7476=CARTESIAN_POINT ( 'NONE',  ( 2.000000000000000000, 0.000000000000000000, 0.000000000000000000 ) ) ;
#7485=ORIENTED_EDGE ( 'NONE', *, *, #777, .T. ) ;
#7496=CIRCLE ( 'NONE', #2182, 2.200000000000001066 ) ;
#7503=DIRECTION ( 'NONE',  ( 0.000000000000000000, 0.000000000000000000, -1.000000000000000000 ) ) ;
#7508=SURFACE_SIDE_STYLE ('',( #4457 ) ) ;
#7521=EDGE_LOOP ( 'NONE', ( #3112, #2247 ) ) ;
#7600=DIRECTION ( 'NONE',  ( -1.000000000000000000, -0.000000000000000000, -0.000000000000000000 ) ) ;
#7613=AXIS2_PLACEMENT_3D ( 'NONE', #6269, #1237, #973 ) ;
#7634=CYLINDRICAL_SURFACE ( 'NONE', #9966, 3.500000000000000000 ) ;
#7645=FILL_AREA_STYLE_COLOUR ( '', #11685 ) ;
#7660=CONICAL_SURFACE ( 'NONE', #7446, 1.535500000000000087, 1.047197551196590748 ) ;
#7683=ORIENTED_EDGE ( 'NONE', *, *, #10131, .T. ) ;
#7700=VECTOR ( 'NONE', #8073, 1000.000000000000227 ) ;
#7723=ORIENTED_EDGE ( 'NONE', *, *, #2977, .F. ) ;
#7736=VECTOR ( 'NONE', #6801, 1000.000000000000000 ) ;
#7764=( LENGTH_UNIT ( ) NAMED_UNIT ( * ) SI_UNIT ( .MILLI., .METRE. ) );
#7779=FACE_OUTER_BOUND ( 'NONE', #13431, .T. ) ;
#7813=ORIENTED_EDGE ( 'NONE', *, *, #13535, .T. ) ;
#7828=EDGE_CURVE ( 'NONE', #2854, #13025, #5131, .T. ) ;
#7840=DIRECTION ( 'NONE',  ( 0.000000000000000000, 0.000000000000000000, -1.000000000000000000 ) ) ;
#7841=AXIS2_PLACEMENT_3D ( 'NONE', #12830, #11802, #11664 ) ;
#7858=ORIENTED_EDGE ( 'NONE', *, *, #4090, .T. ) ;
#7862=PRODUCT_DEFINITION_SHAPE ( 'NONE', 'NONE',  #11484 ) ;
#7894=EDGE_LOOP ( 'NONE', ( #10957, #8491, #3805 ) ) ;
#7905=LINE ( 'NONE', #12186, #3375 ) ;
#7907=VERTEX_POINT ( 'NONE', #9627 ) ;
#7972=EDGE_CURVE ( 'NONE', #2821, #1050, #5346, .T. ) ;
#7989=CARTESIAN_POINT ( 'NONE',  ( 2.000000000000000000, -0.8865213383406730374, -1.535499999999999421 ) ) ;
#7991=AXIS2_PLACEMENT_3D ( 'NONE', #3132, #11696, #10598 ) ;
#7992=AXIS2_PLACEMENT_3D ( 'NONE', #3037, #12505, #7266 ) ;
#8041=EDGE_LOOP ( 'NONE', ( #7042, #5705, #5007 ) ) ;
#8045=VECTOR ( 'NONE', #4798, 1000.000000000000227 ) ;
#8050=DIRECTION ( 'NONE',  ( -1.000000000000000000, -0.000000000000000000, -0.000000000000000000 ) ) ;
#8060=DIRECTION ( 'NONE',  ( 0.000000000000000000, 0.000000000000000000, 1.000000000000000000 ) ) ;
#8073=DIRECTION ( 'NONE',  ( 0.000000000000000000, 0.4999999999999989453, -0.8660254037844391517 ) ) ;
#8087=ADVANCED_FACE ( 'NONE', ( #1307 ), #9531, .T. ) ;
#8102=VECTOR ( 'NONE', #2137, 1000.000000000000000 ) ;
#8104=CARTESIAN_POINT ( 'NONE',  ( 2.000000000000000000, 1.329782007511006281, 0.7677499999999984892 ) ) ;
#8119=CARTESIAN_POINT ( 'NONE',  ( 0.1999999999999987899, 0.000000000000000000, 0.000000000000000000 ) ) ;
#8150=EDGE_CURVE ( 'NONE', #9080, #11927, #11737, .T. ) ;
#8154=ADVANCED_FACE ( 'NONE', ( #12995 ), #10930, .T. ) ;
#8183=ORIENTED_EDGE ( 'NONE', *, *, #12012, .T. ) ;
#8202=ORIENTED_EDGE ( 'NONE', *, *, #4576, .T. ) ;
#8219=ORIENTED_EDGE ( 'NONE', *, *, #5497, .F. ) ;
#8228=VECTOR ( 'NONE', #6202, 1000.000000000000114 ) ;
#8246=CARTESIAN_POINT ( 'NONE',  ( 0.000000000000000000, 0.8865213383406680414, -1.535500000000000975 ) ) ;
#8268=DIRECTION ( 'NONE',  ( 0.000000000000000000, 0.000000000000000000, 1.000000000000000000 ) ) ;
#8310=ADVANCED_FACE ( 'NONE', ( #13195 ), #12379, .T. ) ;
#8316=DIRECTION ( 'NONE',  ( 0.000000000000000000, 0.000000000000000000, 1.000000000000000000 ) ) ;
#8328=ORIENTED_EDGE ( 'NONE', *, *, #9081, .T. ) ;
#8330=DIRECTION ( 'NONE',  ( 0.000000000000000000, 1.000000000000000000, -1.345283343056720273E-15 ) ) ;
#8343=ORIENTED_EDGE ( 'NONE', *, *, #6133, .T. ) ;
#8366=EDGE_CURVE ( 'NONE', #2486, #568, #8997, .T. ) ;
#8392=CARTESIAN_POINT ( 'NONE',  ( 13.61000000000001009, 2.449293598294708386E-16, -2.000000000000001332 ) ) ;
#8412=ORIENTED_EDGE ( 'NONE', *, *, #13535, .F. ) ;
#8444=DIRECTION ( 'NONE',  ( -1.000000000000000000, -0.000000000000000000, -0.000000000000000000 ) ) ;
#8456=CARTESIAN_POINT ( 'NONE',  ( 2.000000000000000000, -0.8865213383406694847, 1.535500000000001419 ) ) ;
#8467=CLOSED_SHELL ( 'NONE', ( #1438, #13446, #5777, #8087, #12924, #8154, #9549, #5215, #11704, #1093, #13107, #6038, #10099, #6293, #2803, #6273, #8310, #2451, #9522, #5034, #11431, #654, #4127, #10081, #9238, #2964, #6784 ) ) ;
#8491=ORIENTED_EDGE ( 'NONE', *, *, #6924, .T. ) ;
#8512=DIRECTION ( 'NONE',  ( 0.000000000000000000, -0.5000000000000011102, -0.8660254037844379305 ) ) ;
#8515=DIRECTION ( 'NONE',  ( 0.000000000000000000, 0.000000000000000000, 1.000000000000000000 ) ) ;
#8521=ORIENTED_EDGE ( 'NONE', *, *, #6133, .F. ) ;
#8543=ORIENTED_EDGE ( 'NONE', *, *, #13177, .T. ) ;
#8545=DIRECTION ( 'NONE',  ( -1.000000000000000000, -0.000000000000000000, -0.000000000000000000 ) ) ;
#8560=DIRECTION ( 'NONE',  ( 0.000000000000000000, 0.000000000000000000, -1.000000000000000000 ) ) ;
#8576=LINE ( 'NONE', #4632, #5989 ) ;
#8582=AXIS2_PLACEMENT_3D ( 'NONE', #3369, #2385, #6364 ) ;
#8603=EDGE_LOOP ( 'NONE', ( #3465, #3264, #10888, #4253 ) ) ;
#8604=STYLED_ITEM ( 'NONE', ( #9582 ), #9629 ) ;
#8623=ORIENTED_EDGE ( 'NONE', *, *, #5805, .F. ) ;
#8642=CARTESIAN_POINT ( 'NONE',  ( 2.000000000000000000, -1.502314598737159426E-15, -1.535500000000000087 ) ) ;
#8664=DIRECTION ( 'NONE',  ( -1.000000000000000000, -0.000000000000000000, -0.000000000000000000 ) ) ;
#8672=FACE_OUTER_BOUND ( 'NONE', #9685, .T. ) ;
#8681=CARTESIAN_POINT ( 'NONE',  ( 4.000000000000003553, 0.000000000000000000, 3.500000000000000000 ) ) ;
#8688=DIRECTION ( 'NONE',  ( -1.000000000000000000, -0.000000000000000000, -0.000000000000000000 ) ) ;
#8708=EDGE_CURVE ( 'NONE', #10184, #11343, #8576, .T. ) ;
#8713=LINE ( 'NONE', #6644, #10709 ) ;
#8727=ORIENTED_EDGE ( 'NONE', *, *, #10836, .F. ) ;
#8730=VERTEX_POINT ( 'NONE', #8780 ) ;
#8740=DIRECTION ( 'NONE',  ( -1.000000000000000000, -0.000000000000000000, -0.000000000000000000 ) ) ;
#8776=CARTESIAN_POINT ( 'NONE',  ( 0.000000000000000000, 0.8865213383406680414, -1.535500000000000975 ) ) ;
#8780=CARTESIAN_POINT ( 'NONE',  ( 2.000000000000000000, -0.8865213383406694847, 1.535500000000001419 ) ) ;
#8785=LINE ( 'NONE', #340, #4710 ) ;
#8828=ORIENTED_EDGE ( 'NONE', *, *, #9649, .F. ) ;
#8838=CARTESIAN_POINT ( 'NONE',  ( 0.000000000000000000, -0.8865213383406730374, -1.535499999999999421 ) ) ;
#8844=AXIS2_PLACEMENT_3D ( 'NONE', #11668, #2192, #6436 ) ;
#8872=AXIS2_PLACEMENT_3D ( 'NONE', #9891, #5622, #6792 ) ;
#8891=CARTESIAN_POINT ( 'NONE',  ( 14.00000000000000000, 1.610000000000000098, 0.000000000000000000 ) ) ;
#8898=ORIENTED_EDGE ( 'NONE', *, *, #1500, .T. ) ;
#8899=AXIS2_PLACEMENT_3D ( 'NONE', #2429, #10674, #7840 ) ;
#8904=CARTESIAN_POINT ( 'NONE',  ( 2.886521338340684917, 0.000000000000000000, 0.000000000000000000 ) ) ;
#8923=DIRECTION ( 'NONE',  ( 1.000000000000000000, 0.000000000000000000, 0.000000000000000000 ) ) ;
#8949=LINE ( 'NONE', #491, #8045 ) ;
#8995=CARTESIAN_POINT ( 'NONE',  ( 0.000000000000000000, -0.8865213383406694847, 1.535500000000001419 ) ) ;
#8997=LINE ( 'NONE', #9277, #10618 ) ;
#9010=DIRECTION ( 'NONE',  ( 0.000000000000000000, 0.000000000000000000, 1.000000000000000000 ) ) ;
#9019=DIRECTION ( 'NONE',  ( 0.000000000000000000, -0.4999999999999989453, 0.8660254037844391517 ) ) ;
#9020=DIRECTION ( 'NONE',  ( -0.000000000000000000, 1.345283343056720273E-15, 1.000000000000000000 ) ) ;
#9023=DIRECTION ( 'NONE',  ( 1.000000000000000000, 0.000000000000000000, 0.000000000000000000 ) ) ;
#9080=VERTEX_POINT ( 'NONE', #2026 ) ;
#9081=EDGE_CURVE ( 'NONE', #568, #3385, #3744, .T. ) ;
#9105=DIRECTION ( 'NONE',  ( 0.000000000000000000, -1.000000000000000000, 9.783878858594328898E-16 ) ) ;
#9152=ORIENTED_EDGE ( 'NONE', *, *, #1798, .T. ) ;
#9168=DIRECTION ( 'NONE',  ( 0.000000000000000000, 0.000000000000000000, -1.000000000000000000 ) ) ;
#9178=CARTESIAN_POINT ( 'NONE',  ( 0.000000000000000000, -0.8865213383406694847, 1.535500000000001419 ) ) ;
#9207=CIRCLE ( 'NONE', #5199, 2.000000000000001332 ) ;
#9238=ADVANCED_FACE ( 'NONE', ( #10914 ), #5677, .F. ) ;
#9259=AXIS2_PLACEMENT_3D ( 'NONE', #7060, #3809, #10232 ) ;
#9277=CARTESIAN_POINT ( 'NONE',  ( -31.74999999999995737, 0.000000000000000000, 2.000000000000000888 ) ) ;
#9280=AXIS2_PLACEMENT_3D ( 'NONE', #2063, #12432, #3175 ) ;
#9289=VERTEX_POINT ( 'NONE', #6777 ) ;
#9318=LINE ( 'NONE', #4061, #7410 ) ;
#9321=AXIS2_PLACEMENT_3D ( 'NONE', #1445, #2422, #5691 ) ;
#9338=DIRECTION ( 'NONE',  ( -1.000000000000000000, -0.000000000000000000, -0.000000000000000000 ) ) ;
#9344=FACE_OUTER_BOUND ( 'NONE', #7521, .T. ) ;
#9354=VECTOR ( 'NONE', #9338, 1000.000000000000000 ) ;
#9406=DIRECTION ( 'NONE',  ( 1.000000000000000000, 0.000000000000000000, 0.000000000000000000 ) ) ;
#9410=CARTESIAN_POINT ( 'NONE',  ( 4.000000000000000000, 3.500000000000000000, 0.000000000000000000 ) ) ;
#9430=DIRECTION ( 'NONE',  ( 0.000000000000000000, 1.224646799147353207E-16, 1.000000000000000000 ) ) ;
#9432=PLANE ( 'NONE',  #471 ) ;
#9445=( NAMED_UNIT ( * ) SI_UNIT ( $, .STERADIAN. ) SOLID_ANGLE_UNIT ( ) );
#9463=PLANE ( 'NONE',  #9280 ) ;
#9480=CARTESIAN_POINT ( 'NONE',  ( 4.000000000000001776, 2.694222958124178486E-16, 2.200000000000001066 ) ) ;
#9486=VERTEX_POINT ( 'NONE', #9604 ) ;
#9507=EDGE_LOOP ( 'NONE', ( #5923, #1630, #2978, #2333 ) ) ;
#9522=ADVANCED_FACE ( 'NONE', ( #6370 ), #9463, .F. ) ;
#9531=CONICAL_SURFACE ( 'NONE', #8872, 1.610000000000000098, 0.7853981633974658205 ) ;
#9549=ADVANCED_FACE ( 'NONE', ( #3105, #13530 ), #4077, .T. ) ;
#9555=ORIENTED_EDGE ( 'NONE', *, *, #1362, .F. ) ;
#9582=PRESENTATION_STYLE_ASSIGNMENT (( #106 ) ) ;
#9592=LINE ( 'NONE', #12370, #9354 ) ;
#9602=AXIS2_PLACEMENT_3D ( 'NONE', #11091, #9023, #9168 ) ;
#9604=CARTESIAN_POINT ( 'NONE',  ( 4.000000000000001776, 0.000000000000000000, -2.200000000000001066 ) ) ;
#9627=CARTESIAN_POINT ( 'NONE',  ( 13.99999999999999822, 0.000000000000000000, 1.610000000000000098 ) ) ;
#9629=ADVANCED_BREP_SHAPE_REPRESENTATION ( '', ( #1187, #430 ), #3078 ) ;
#9649=EDGE_CURVE ( 'NONE', #11305, #6619, #3971, .T. ) ;
#9683=AXIS2_PLACEMENT_3D ( 'NONE', #1756, #3015, #11381 ) ;
#9685=EDGE_LOOP ( 'NONE', ( #13244, #7423, #7485, #2506, #4588 ) ) ;
#9688=VERTEX_POINT ( 'NONE', #8838 ) ;
#9702=CARTESIAN_POINT ( 'NONE',  ( 0.000000000000000000, 0.000000000000000000, 3.299999999999999822 ) ) ;
#9809=VERTEX_POINT ( 'NONE', #9178 ) ;
#9838=DIRECTION ( 'NONE',  ( 0.000000000000000000, 0.4999999999999991118, -0.8660254037844390407 ) ) ;
#9856=ORIENTED_EDGE ( 'NONE', *, *, #13515, .T. ) ;
#9863=DIRECTION ( 'NONE',  ( -1.000000000000000000, -0.000000000000000000, -0.000000000000000000 ) ) ;
#9886=VECTOR ( 'NONE', #10168, 1000.000000000000000 ) ;
#9887=VERTEX_POINT ( 'NONE', #5800 ) ;
#9891=CARTESIAN_POINT ( 'NONE',  ( 13.99999999999999822, 0.000000000000000000, 0.000000000000000000 ) ) ;
#9926=LINE ( 'NONE', #6822, #4254 ) ;
#9960=CARTESIAN_POINT ( 'NONE',  ( 2.000000000000000000, 0.000000000000000000, 0.000000000000000000 ) ) ;
#9964=AXIS2_PLACEMENT_3D ( 'NONE', #9960, #8664, #2285 ) ;
#9966=AXIS2_PLACEMENT_3D ( 'NONE', #2294, #8740, #11905 ) ;
#9979=CARTESIAN_POINT ( 'NONE',  ( 0.1999999999999987899, 0.000000000000000000, 0.000000000000000000 ) ) ;
#10006=VERTEX_POINT ( 'NONE', #11653 ) ;
#10033=DIRECTION ( 'NONE',  ( 0.000000000000000000, 0.000000000000000000, -1.000000000000000000 ) ) ;
#10040=DIRECTION ( 'NONE',  ( -1.000000000000000000, -0.000000000000000000, -0.000000000000000000 ) ) ;
#10045=DIRECTION ( 'NONE',  ( -0.7071067811865350272, 0.000000000000000000, 0.7071067811865598962 ) ) ;
#10046=DIRECTION ( 'NONE',  ( -0.000000000000000000, 0.8660254037844392627, 0.4999999999999990008 ) ) ;
#10047=FACE_OUTER_BOUND ( 'NONE', #11631, .T. ) ;
#10081=ADVANCED_FACE ( 'NONE', ( #1201 ), #10810, .F. ) ;
#10091=FACE_OUTER_BOUND ( 'NONE', #3466, .T. ) ;
#10099=ADVANCED_FACE ( 'NONE', ( #11919 ), #2203, .F. ) ;
#10115=PLANE ( 'NONE',  #136 ) ;
#10116=DIRECTION ( 'NONE',  ( 0.000000000000000000, -1.000000000000000000, 1.345283343056720273E-15 ) ) ;
#10131=EDGE_CURVE ( 'NONE', #8730, #11305, #3201, .T. ) ;
#10132=( GEOMETRIC_REPRESENTATION_CONTEXT ( 3 ) GLOBAL_UNCERTAINTY_ASSIGNED_CONTEXT ( ( #12954 ) ) GLOBAL_UNIT_ASSIGNED_CONTEXT ( ( #6354, #10747, #10684 ) ) REPRESENTATION_CONTEXT ( 'NONE', 'WORKASPACE' ) );
#10155=AXIS2_PLACEMENT_3D ( 'NONE', #2531, #7600, #324 ) ;
#10168=DIRECTION ( 'NONE',  ( 0.000000000000000000, 1.000000000000000000, -1.345283343056720273E-15 ) ) ;
#10184=VERTEX_POINT ( 'NONE', #4170 ) ;
#10196=LINE ( 'NONE', #7989, #517 ) ;
#10197=VERTEX_POINT ( 'NONE', #8392 ) ;
#10232=DIRECTION ( 'NONE',  ( 0.000000000000000000, 0.000000000000000000, -1.000000000000000000 ) ) ;
#10245=ORIENTED_EDGE ( 'NONE', *, *, #12989, .T. ) ;
#10300=EDGE_LOOP ( 'NONE', ( #2647, #6706, #11287, #2332, #9152 ) ) ;
#10325=SHAPE_DEFINITION_REPRESENTATION ( #7862, #7264 ) ;
#10333=DIRECTION ( 'NONE',  ( -1.000000000000000000, -0.000000000000000000, -0.000000000000000000 ) ) ;
#10342=( NAMED_UNIT ( * ) PLANE_ANGLE_UNIT ( ) SI_UNIT ( $, .RADIAN. ) );
#10359=EDGE_CURVE ( 'NONE', #9809, #3329, #540, .T. ) ;
#10363=VECTOR ( 'NONE', #12883, 1000.000000000000000 ) ;
#10470=CARTESIAN_POINT ( 'NONE',  ( 4.000000000000000000, 0.000000000000000000, 0.000000000000000000 ) ) ;
#10542=VERTEX_POINT ( 'NONE', #8776 ) ;
#10572=EDGE_CURVE ( 'NONE', #5152, #9289, #4608, .T. ) ;
#10580=LINE ( 'NONE', #4094, #2337 ) ;
#10598=DIRECTION ( 'NONE',  ( 0.000000000000000000, 0.000000000000000000, 1.000000000000000000 ) ) ;
#10618=VECTOR ( 'NONE', #13333, 1000.000000000000000 ) ;
#10639=CIRCLE ( 'NONE', #4242, 2.000000000000000888 ) ;
#10644=ORIENTED_EDGE ( 'NONE', *, *, #2561, .F. ) ;
#10674=DIRECTION ( 'NONE',  ( 1.000000000000000000, 0.000000000000000000, 0.000000000000000000 ) ) ;
#10682=LINE ( 'NONE', #10745, #2505 ) ;
#10684=( NAMED_UNIT ( * ) SI_UNIT ( $, .STERADIAN. ) SOLID_ANGLE_UNIT ( ) );
#10704=VECTOR ( 'NONE', #6751, 1000.000000000000000 ) ;
#10709=VECTOR ( 'NONE', #8512, 1000.000000000000114 ) ;
#10733=FACE_OUTER_BOUND ( 'NONE', #7095, .T. ) ;
#10745=CARTESIAN_POINT ( 'NONE',  ( -31.74999999999995737, 4.286263797015736595E-16, -3.500000000000000000 ) ) ;
#10747=( NAMED_UNIT ( * ) PLANE_ANGLE_UNIT ( ) SI_UNIT ( $, .RADIAN. ) );
#10756=ORIENTED_EDGE ( 'NONE', *, *, #1946, .F. ) ;
#10795=FACE_OUTER_BOUND ( 'NONE', #7894, .T. ) ;
#10810=PLANE ( 'NONE',  #3981 ) ;
#10813=CARTESIAN_POINT ( 'NONE',  ( 2.000000000000000000, -0.8865213383406694847, 1.535500000000001419 ) ) ;
#10836=EDGE_CURVE ( 'NONE', #568, #5875, #4164, .T. ) ;
#10867=PLANE ( 'NONE',  #6690 ) ;
#10874=DIRECTION ( 'NONE',  ( -1.000000000000000000, -0.000000000000000000, -0.000000000000000000 ) ) ;
#10878=DIRECTION ( 'NONE',  ( 1.000000000000000000, 0.000000000000000000, 0.000000000000000000 ) ) ;
#10888=ORIENTED_EDGE ( 'NONE', *, *, #1500, .F. ) ;
#10914=FACE_OUTER_BOUND ( 'NONE', #4421, .T. ) ;
#10930=CYLINDRICAL_SURFACE ( 'NONE', #9321, 3.500000000000000000 ) ;
#10946=AXIS2_PLACEMENT_3D ( 'NONE', #12330, #6950, #4880 ) ;
#10957=ORIENTED_EDGE ( 'NONE', *, *, #5113, .T. ) ;
#10972=ORIENTED_EDGE ( 'NONE', *, *, #8366, .T. ) ;
#10978=DIRECTION ( 'NONE',  ( 0.000000000000000000, 0.000000000000000000, -1.000000000000000000 ) ) ;
#10985=ORIENTED_EDGE ( 'NONE', *, *, #12102, .F. ) ;
#10986=VECTOR ( 'NONE', #8330, 1000.000000000000000 ) ;
#10990=DIRECTION ( 'NONE',  ( 0.000000000000000000, 0.000000000000000000, 1.000000000000000000 ) ) ;
#10998=LINE ( 'NONE', #2782, #482 ) ;
#11010=AXIS2_PLACEMENT_3D ( 'NONE', #8891, #242, #305 ) ;
#11022=PRODUCT_DEFINITION_CONTEXT ( 'detailed design', #11126, 'design' ) ;
#11033=LINE ( 'NONE', #12352, #12248 ) ;
#11040=EDGE_LOOP ( 'NONE', ( #10644, #8623, #8202, #8183, #12233 ) ) ;
#11071=ORIENTED_EDGE ( 'NONE', *, *, #12483, .T. ) ;
#11076=VECTOR ( 'NONE', #10045, 1000.000000000000114 ) ;
#11081=EDGE_CURVE ( 'NONE', #7907, #11125, #189, .T. ) ;
#11091=CARTESIAN_POINT ( 'NONE',  ( 2.000000000000000000, 1.773042676681340524, -2.059984127722458425E-15 ) ) ;
#11094=ORIENTED_EDGE ( 'NONE', *, *, #10836, .T. ) ;
#11125=VERTEX_POINT ( 'NONE', #7023 ) ;
#11126=APPLICATION_CONTEXT ( 'automotive_design' ) ;
#11129=AXIS2_PLACEMENT_3D ( 'NONE', #7194, #6162, #11546 ) ;
#11154=LINE ( 'NONE', #3965, #11076 ) ;
#11273=AXIS2_PLACEMENT_3D ( 'NONE', #6043, #1723, #2776 ) ;
#11287=ORIENTED_EDGE ( 'NONE', *, *, #6862, .F. ) ;
#11290=DIRECTION ( 'NONE',  ( 0.000000000000000000, 0.000000000000000000, 1.000000000000000000 ) ) ;
#11305=VERTEX_POINT ( 'NONE', #5501 ) ;
#11317=ORIENTED_EDGE ( 'NONE', *, *, #10572, .T. ) ;
#11343=VERTEX_POINT ( 'NONE', #4322 ) ;
#11360=AXIS2_PLACEMENT_3D ( 'NONE', #365, #10874, #9010 ) ;
#11381=DIRECTION ( 'NONE',  ( 0.000000000000000000, 0.000000000000000000, 1.000000000000000000 ) ) ;
#11385=CARTESIAN_POINT ( 'NONE',  ( 4.200000000000001954, 2.449293598294707893E-16, -2.000000000000000888 ) ) ;
#11412=DIRECTION ( 'NONE',  ( -1.000000000000000000, -0.000000000000000000, -0.000000000000000000 ) ) ;
#11431=ADVANCED_FACE ( 'NONE', ( #10091 ), #6992, .F. ) ;
#11484=PRODUCT_DEFINITION ( 'UNKNOWN', '', #7065, #11022 ) ;
#11506=CARTESIAN_POINT ( 'NONE',  ( 0.000000000000000000, 1.773042676681340524, -2.059984127722458425E-15 ) ) ;
#11512=CARTESIAN_POINT ( 'NONE',  ( 2.000000000000000000, 1.773042676681340524, -2.059984127722458425E-15 ) ) ;
#11523=ORIENTED_EDGE ( 'NONE', *, *, #1344, .F. ) ;
#11546=DIRECTION ( 'NONE',  ( 0.000000000000000000, 0.000000000000000000, 1.000000000000000000 ) ) ;
#11585=AXIS2_PLACEMENT_3D ( 'NONE', #8119, #1739, #12322 ) ;
#11621=CARTESIAN_POINT ( 'NONE',  ( 2.000000000000000000, 0.000000000000000000, 0.000000000000000000 ) ) ;
#11623=LINE ( 'NONE', #8246, #8102 ) ;
#11631=EDGE_LOOP ( 'NONE', ( #6525, #1682, #8521, #922, #12657 ) ) ;
#11653=CARTESIAN_POINT ( 'NONE',  ( 2.000000000000000000, 0.8865213383406680414, -1.535500000000000975 ) ) ;
#11657=FACE_OUTER_BOUND ( 'NONE', #3887, .T. ) ;
#11664=DIRECTION ( 'NONE',  ( 0.000000000000000000, 0.000000000000000000, 1.000000000000000000 ) ) ;
#11668=CARTESIAN_POINT ( 'NONE',  ( 0.000000000000000000, 0.000000000000000000, 0.000000000000000000 ) ) ;
#11679=AXIS2_PLACEMENT_3D ( 'NONE', #4806, #9020, #10116 ) ;
#11685=COLOUR_RGB ( '',1.000000000000000000, 0.9490196078431372140, 0.9098039215686274384 ) ;
#11695=LINE ( 'NONE', #11506, #11799 ) ;
#11696=DIRECTION ( 'NONE',  ( -1.000000000000000000, -0.000000000000000000, -0.000000000000000000 ) ) ;
#11704=ADVANCED_FACE ( 'NONE', ( #2909, #9344 ), #5208, .T. ) ;
#11708=AXIS2_PLACEMENT_3D ( 'NONE', #6680, #10878, #1392 ) ;
#11712=EDGE_LOOP ( 'NONE', ( #5613, #7683, #10756 ) ) ;
#11737=CIRCLE ( 'NONE', #9964, 1.535500000000000087 ) ;
#11746=AXIS2_PLACEMENT_3D ( 'NONE', #11621, #11412, #1986 ) ;
#11763=ORIENTED_EDGE ( 'NONE', *, *, #6379, .F. ) ;
#11799=VECTOR ( 'NONE', #2021, 1000.000000000000000 ) ;
#11802=DIRECTION ( 'NONE',  ( -1.000000000000000000, -0.000000000000000000, -0.000000000000000000 ) ) ;
#11866=CARTESIAN_POINT ( 'NONE',  ( 2.000000000000000000, -1.773042676681341856, 2.276824562219559311E-15 ) ) ;
#11868=LINE ( 'NONE', #1215, #13328 ) ;
#11905=DIRECTION ( 'NONE',  ( 0.000000000000000000, 0.000000000000000000, 1.000000000000000000 ) ) ;
#11919=FACE_OUTER_BOUND ( 'NONE', #9507, .T. ) ;
#11927=VERTEX_POINT ( 'NONE', #8642 ) ;
#11990=CARTESIAN_POINT ( 'NONE',  ( 13.99999999999999822, 0.000000000000000000, 0.000000000000000000 ) ) ;
#12012=EDGE_CURVE ( 'NONE', #2436, #7271, #8713, .T. ) ;
#12057=DIRECTION ( 'NONE',  ( 0.000000000000000000, 0.000000000000000000, 1.000000000000000000 ) ) ;
#12071=ORIENTED_EDGE ( 'NONE', *, *, #1404, .F. ) ;
#12080=DIRECTION ( 'NONE',  ( 0.000000000000000000, -0.5000000000000011102, -0.8660254037844379305 ) ) ;
#12101=ORIENTED_EDGE ( 'NONE', *, *, #13109, .T. ) ;
#12102=EDGE_CURVE ( 'NONE', #13025, #5152, #12294, .T. ) ;
#12118=ORIENTED_EDGE ( 'NONE', *, *, #2465, .T. ) ;
#12177=( NAMED_UNIT ( * ) SI_UNIT ( $, .STERADIAN. ) SOLID_ANGLE_UNIT ( ) );
#12186=CARTESIAN_POINT ( 'NONE',  ( 2.000000000000000000, 1.880445160090761061E-16, -1.535500000000000087 ) ) ;
#12187=CIRCLE ( 'NONE', #6024, 3.299999999999999822 ) ;
#12197=CARTESIAN_POINT ( 'NONE',  ( 2.000000000000000000, -1.773042676681341856, 2.276824562219559311E-15 ) ) ;
#12233=ORIENTED_EDGE ( 'NONE', *, *, #6966, .T. ) ;
#12238=CIRCLE ( 'NONE', #7841, 1.535500000000000087 ) ;
#12248=VECTOR ( 'NONE', #12080, 1000.000000000000114 ) ;
#12250=CARTESIAN_POINT ( 'NONE',  ( 4.200000000000001954, 0.000000000000000000, 0.000000000000000000 ) ) ;
#12287=EDGE_LOOP ( 'NONE', ( #6887, #8219 ) ) ;
#12294=LINE ( 'NONE', #460, #970 ) ;
#12322=DIRECTION ( 'NONE',  ( 0.000000000000000000, 0.000000000000000000, 1.000000000000000000 ) ) ;
#12330=CARTESIAN_POINT ( 'NONE',  ( 4.000000000000003553, 0.000000000000000000, 0.000000000000000000 ) ) ;
#12352=CARTESIAN_POINT ( 'NONE',  ( 2.000000000000000000, -0.8865213383406694847, 1.535500000000001419 ) ) ;
#12370=CARTESIAN_POINT ( 'NONE',  ( 2.000000000000000000, 0.8865213383406715941, 1.535499999999999199 ) ) ;
#12373=ORIENTED_EDGE ( 'NONE', *, *, #2561, .T. ) ;
#12379=PLANE ( 'NONE',  #11273 ) ;
#12391=EDGE_LOOP ( 'NONE', ( #4204, #793 ) ) ;
#12415=VECTOR ( 'NONE', #9863, 1000.000000000000000 ) ;
#12432=DIRECTION ( 'NONE',  ( 0.000000000000000000, -9.783878858594328898E-16, -1.000000000000000000 ) ) ;
#12483=EDGE_CURVE ( 'NONE', #9289, #1050, #5209, .T. ) ;
#12504=CIRCLE ( 'NONE', #3247, 3.500000000000000000 ) ;
#12505=DIRECTION ( 'NONE',  ( -1.000000000000000000, -0.000000000000000000, -0.000000000000000000 ) ) ;
#12543=CARTESIAN_POINT ( 'NONE',  ( 2.000000000000000000, 0.000000000000000000, 0.000000000000000000 ) ) ;
#12556=LINE ( 'NONE', #7175, #6176 ) ;
#12582=DIRECTION ( 'NONE',  ( 0.000000000000000000, 0.000000000000000000, -1.000000000000000000 ) ) ;
#12586=LINE ( 'NONE', #5340, #6775 ) ;
#12608=LINE ( 'NONE', #2937, #3016 ) ;
#12619=CYLINDRICAL_SURFACE ( 'NONE', #117, 2.000000000000000888 ) ;
#12657=ORIENTED_EDGE ( 'NONE', *, *, #5805, .T. ) ;
#12670=DIRECTION ( 'NONE',  ( -1.000000000000000000, -0.000000000000000000, -0.000000000000000000 ) ) ;
#12681=AXIS2_PLACEMENT_3D ( 'NONE', #57, #12701, #1688 ) ;
#12699=DIRECTION ( 'NONE',  ( 0.000000000000000000, -1.224646799147353207E-16, 1.000000000000000000 ) ) ;
#12701=DIRECTION ( 'NONE',  ( -1.000000000000000000, -0.000000000000000000, -0.000000000000000000 ) ) ;
#12767=AXIS2_PLACEMENT_3D ( 'NONE', #6906, #4765, #13043 ) ;
#12772=ORIENTED_EDGE ( 'NONE', *, *, #6862, .T. ) ;
#12806=CARTESIAN_POINT ( 'NONE',  ( 2.000000000000000000, 1.773042676681340524, -2.059984127722458425E-15 ) ) ;
#12807=ORIENTED_EDGE ( 'NONE', *, *, #1798, .F. ) ;
#12816=CARTESIAN_POINT ( 'NONE',  ( 4.000000000000000000, 0.000000000000000000, 0.000000000000000000 ) ) ;
#12829=CARTESIAN_POINT ( 'NONE',  ( 4.200000000000001954, 0.000000000000000000, -2.200000000000001066 ) ) ;
#12830=CARTESIAN_POINT ( 'NONE',  ( 2.000000000000000000, 0.000000000000000000, 0.000000000000000000 ) ) ;
#12862=CARTESIAN_POINT ( 'NONE',  ( 0.000000000000000000, 4.163799117101000559E-16, -3.299999999999999822 ) ) ;
#12874=CARTESIAN_POINT ( 'NONE',  ( -31.74999999999995737, 0.000000000000000000, 0.000000000000000000 ) ) ;
#12876=SHAPE_REPRESENTATION_RELATIONSHIP ( 'NONE' , 'NONE' ,  #7264, #9629 ) ;
#12881=TOROIDAL_SURFACE ( 'NONE', #11585, 3.299999999999999822, 0.2000000000000000111 ) ;
#12883=DIRECTION ( 'NONE',  ( 0.000000000000000000, 1.000000000000000000, -1.345283343056720273E-15 ) ) ;
#12884=DIRECTION ( 'NONE',  ( 0.000000000000000000, 0.000000000000000000, -1.000000000000000000 ) ) ;
#12905=AXIS2_PLACEMENT_3D ( 'NONE', #5460, #316, #12699 ) ;
#12924=ADVANCED_FACE ( 'NONE', ( #36 ), #12619, .T. ) ;
#12954=UNCERTAINTY_MEASURE_WITH_UNIT (LENGTH_MEASURE( 1.000000000000000082E-05 ), #6354, 'distance_accuracy_value', 'NONE');
#12981=CARTESIAN_POINT ( 'NONE',  ( 2.000000000000000000, 1.773042676681340524, -2.059984127722458425E-15 ) ) ;
#12988=ORIENTED_EDGE ( 'NONE', *, *, #5441, .T. ) ;
#12989=EDGE_CURVE ( 'NONE', #2854, #9289, #10682, .T. ) ;
#12993=ORIENTED_EDGE ( 'NONE', *, *, #2977, .T. ) ;
#12995=FACE_OUTER_BOUND ( 'NONE', #4033, .T. ) ;
#13025=VERTEX_POINT ( 'NONE', #8681 ) ;
#13043=DIRECTION ( 'NONE',  ( 0.000000000000000000, 0.000000000000000000, 1.000000000000000000 ) ) ;
#13068=VECTOR ( 'NONE', #13099, 1000.000000000000000 ) ;
#13086=CARTESIAN_POINT ( 'NONE',  ( 13.61000000000001009, 0.000000000000000000, 2.000000000000001332 ) ) ;
#13099=DIRECTION ( 'NONE',  ( 0.000000000000000000, -1.000000000000000000, 9.783878858594328898E-16 ) ) ;
#13107=ADVANCED_FACE ( 'NONE', ( #7779 ), #1185, .T. ) ;
#13109=EDGE_CURVE ( 'NONE', #7271, #2163, #8949, .T. ) ;
#13113=ORIENTED_EDGE ( 'NONE', *, *, #10359, .F. ) ;
#13163=CARTESIAN_POINT ( 'NONE',  ( 2.000000000000000000, 0.8865213383406680414, -1.535500000000000975 ) ) ;
#13177=EDGE_CURVE ( 'NONE', #2163, #2436, #3631, .T. ) ;
#13195=FACE_OUTER_BOUND ( 'NONE', #11040, .T. ) ;
#13232=DIRECTION ( 'NONE',  ( -1.000000000000000000, -0.000000000000000000, -0.000000000000000000 ) ) ;
#13244=ORIENTED_EDGE ( 'NONE', *, *, #13515, .F. ) ;
#13249=AXIS2_PLACEMENT_3D ( 'NONE', #6272, #5229, #9430 ) ;
#13328=VECTOR ( 'NONE', #6433, 1000.000000000000000 ) ;
#13333=DIRECTION ( 'NONE',  ( -1.000000000000000000, -0.000000000000000000, -0.000000000000000000 ) ) ;
#13394=ORIENTED_EDGE ( 'NONE', *, *, #4766, .T. ) ;
#13431=EDGE_LOOP ( 'NONE', ( #5471, #1662, #2449, #13483 ) ) ;
#13434=TOROIDAL_SURFACE ( 'NONE', #13655, 3.299999999999999822, 0.2000000000000000111 ) ;
#13446=ADVANCED_FACE ( 'NONE', ( #7154 ), #12881, .T. ) ;
#13483=ORIENTED_EDGE ( 'NONE', *, *, #1613, .F. ) ;
#13515=EDGE_CURVE ( 'NONE', #11343, #3329, #11695, .T. ) ;
#13516=EDGE_LOOP ( 'NONE', ( #8898, #7472, #12988, #1541 ) ) ;
#13530=FACE_OUTER_BOUND ( 'NONE', #12391, .T. ) ;
#13535=EDGE_CURVE ( 'NONE', #5152, #2821, #958, .T. ) ;
#13552=CIRCLE ( 'NONE', #11129, 2.000000000000001332 ) ;
#13655=AXIS2_PLACEMENT_3D ( 'NONE', #9979, #701, #8060 ) ;
#13706=COLOUR_RGB('Black',0.12,0.14,0.17);
#13707=FILL_AREA_STYLE_COLOUR('',#13706);
#13708=FILL_AREA_STYLE('',(#13707));
#13709=SURFACE_STYLE_FILL_AREA(#13708);
#13710=SURFACE_SIDE_STYLE('',(#13709));
#13711=SURFACE_STYLE_USAGE(.BOTH.,#13710);
#13712=PRESENTATION_STYLE_ASSIGNMENT((#13711));
ENDSEC;
END-ISO-10303-21;
